ISO-10303-21;
HEADER;
/* Generated by software containing ST-Developer
 * from STEP Tools, Inc. (www.steptools.com) 
 */

FILE_DESCRIPTION(
/* description */ ('Hand wheel with handle and shaft collar'),
/* implementation_level */ '2;1');

FILE_NAME(
/* name */ 'Flat Washer - M6.step',
/* time_stamp */ '2026-10-28T03:23:19-07:00',
/* author */ (''),
/* organization */ (''),
/* preprocessor_version */ 'ST-DEVELOPER v20.2',
/* originating_system */ 'Autodesk Translation Framework v15.17.0.0',
/* authorisation */ '');

FILE_SCHEMA (('AUTOMOTIVE_DESIGN { 1 0 10303 214 3 1 1 }'));
ENDSEC;

DATA;
#10=MECHANICAL_DESIGN_GEOMETRIC_PRESENTATION_REPRESENTATION('',(#402),#10510);
#338=SHAPE_REPRESENTATION_RELATIONSHIP('SRR','None',#10654,#370);
#370=ADVANCED_BREP_SHAPE_REPRESENTATION('',(#449),#10481);
#402=STYLED_ITEM('',(#10915),#449);
#449=MANIFOLD_SOLID_BREP('Body1',#5301);
#536=FACE_BOUND('',#1200,.T.);
#537=FACE_BOUND('',#1202,.T.);
#634=PLANE('',#5836);
#635=PLANE('',#5837);
#828=FACE_OUTER_BOUND('',#1197,.T.);
#829=FACE_OUTER_BOUND('',#1198,.T.);
#830=FACE_OUTER_BOUND('',#1199,.T.);
#831=FACE_OUTER_BOUND('',#1201,.T.);
#1197=EDGE_LOOP('',(#3851,#3852,#3853,#3854));
#1198=EDGE_LOOP('',(#3855,#3856,#3857,#3858));
#1199=EDGE_LOOP('',(#3859));
#1200=EDGE_LOOP('',(#3860));
#1201=EDGE_LOOP('',(#3861));
#1202=EDGE_LOOP('',(#3862));
#1602=LINE('',#8497,#1912);
#1603=LINE('',#8503,#1913);
#1912=VECTOR('',#6778,0.32);
#1913=VECTOR('',#6785,0.6);
#2191=CIRCLE('',#5831,0.32);
#2192=CIRCLE('',#5832,0.32);
#2193=CIRCLE('',#5834,0.6);
#2194=CIRCLE('',#5835,0.6);
#2542=VERTEX_POINT('',#8494);
#2543=VERTEX_POINT('',#8496);
#2544=VERTEX_POINT('',#8500);
#2545=VERTEX_POINT('',#8502);
#3043=EDGE_CURVE('',#2542,#2542,#2191,.T.);
#3044=EDGE_CURVE('',#2542,#2543,#1602,.T.);
#3045=EDGE_CURVE('',#2543,#2543,#2192,.T.);
#3046=EDGE_CURVE('',#2544,#2544,#2193,.T.);
#3047=EDGE_CURVE('',#2544,#2545,#1603,.T.);
#3048=EDGE_CURVE('',#2545,#2545,#2194,.T.);
#3851=ORIENTED_EDGE('',*,*,#3043,.F.);
#3852=ORIENTED_EDGE('',*,*,#3044,.T.);
#3853=ORIENTED_EDGE('',*,*,#3045,.T.);
#3854=ORIENTED_EDGE('',*,*,#3044,.F.);
#3855=ORIENTED_EDGE('',*,*,#3046,.F.);
#3856=ORIENTED_EDGE('',*,*,#3047,.T.);
#3857=ORIENTED_EDGE('',*,*,#3048,.T.);
#3858=ORIENTED_EDGE('',*,*,#3047,.F.);
#3859=ORIENTED_EDGE('',*,*,#3046,.T.);
#3860=ORIENTED_EDGE('',*,*,#3043,.T.);
#3861=ORIENTED_EDGE('',*,*,#3048,.F.);
#3862=ORIENTED_EDGE('',*,*,#3045,.F.);
#4908=CYLINDRICAL_SURFACE('',#5830,0.32);
#4909=CYLINDRICAL_SURFACE('',#5833,0.6);
#5040=ADVANCED_FACE('',(#828),#4908,.F.);
#5041=ADVANCED_FACE('',(#829),#4909,.T.);
#5042=ADVANCED_FACE('',(#830,#536),#634,.T.);
#5043=ADVANCED_FACE('',(#831,#537),#635,.F.);
#5301=CLOSED_SHELL('',(#5040,#5041,#5042,#5043));
#5829=AXIS2_PLACEMENT_3D('',#8492,#6772,#6773);
#5830=AXIS2_PLACEMENT_3D('',#8493,#6774,#6775);
#5831=AXIS2_PLACEMENT_3D('',#8495,#6776,#6777);
#5832=AXIS2_PLACEMENT_3D('',#8498,#6779,#6780);
#5833=AXIS2_PLACEMENT_3D('',#8499,#6781,#6782);
#5834=AXIS2_PLACEMENT_3D('',#8501,#6783,#6784);
#5835=AXIS2_PLACEMENT_3D('',#8504,#6786,#6787);
#5836=AXIS2_PLACEMENT_3D('',#8505,#6788,#6789);
#5837=AXIS2_PLACEMENT_3D('',#8506,#6790,#6791);
#6772=DIRECTION('axis',(0.,0.,1.));
#6773=DIRECTION('refdir',(1.,0.,0.));
#6774=DIRECTION('center_axis',(0.,1.,0.));
#6775=DIRECTION('ref_axis',(1.,0.,0.));
#6776=DIRECTION('center_axis',(0.,-1.,0.));
#6777=DIRECTION('ref_axis',(1.,0.,0.));
#6778=DIRECTION('',(0.,-1.,0.));
#6779=DIRECTION('center_axis',(0.,-1.,0.));
#6780=DIRECTION('ref_axis',(1.,0.,0.));
#6781=DIRECTION('center_axis',(0.,1.,0.));
#6782=DIRECTION('ref_axis',(1.,0.,0.));
#6783=DIRECTION('center_axis',(0.,1.,0.));
#6784=DIRECTION('ref_axis',(1.,0.,0.));
#6785=DIRECTION('',(0.,-1.,0.));
#6786=DIRECTION('center_axis',(0.,1.,0.));
#6787=DIRECTION('ref_axis',(1.,0.,0.));
#6788=DIRECTION('center_axis',(0.,1.,0.));
#6789=DIRECTION('ref_axis',(1.,0.,0.));
#6790=DIRECTION('center_axis',(0.,1.,0.));
#6791=DIRECTION('ref_axis',(1.,0.,0.));
#8492=CARTESIAN_POINT('',(0.,0.,0.));
#8493=CARTESIAN_POINT('Origin',(0.,0.,0.));
#8494=CARTESIAN_POINT('',(-0.32,0.16,3.91886975727153E-17));
#8495=CARTESIAN_POINT('Origin',(0.,0.16,0.));
#8496=CARTESIAN_POINT('',(-0.32,0.,3.91886975727153E-17));
#8497=CARTESIAN_POINT('',(-0.32,0.,3.91886975727153E-17));
#8498=CARTESIAN_POINT('Origin',(0.,0.,0.));
#8499=CARTESIAN_POINT('Origin',(0.,0.,0.));
#8500=CARTESIAN_POINT('',(-0.6,0.16,7.34788079488412E-17));
#8501=CARTESIAN_POINT('Origin',(0.,0.16,0.));
#8502=CARTESIAN_POINT('',(-0.6,0.,7.34788079488412E-17));
#8503=CARTESIAN_POINT('',(-0.6,0.,7.34788079488412E-17));
#8504=CARTESIAN_POINT('Origin',(0.,0.,0.));
#8505=CARTESIAN_POINT('Origin',(0.,0.16,0.));
#8506=CARTESIAN_POINT('Origin',(0.,0.,0.));
#10442=UNCERTAINTY_MEASURE_WITH_UNIT(LENGTH_MEASURE(0.001),#10511,
'DISTANCE_ACCURACY_VALUE',
'Maximum model space distance between geometric entities at asserted c
onnectivities');
#10471=UNCERTAINTY_MEASURE_WITH_UNIT(LENGTH_MEASURE(0.001),#10511,
'DISTANCE_ACCURACY_VALUE',
'Maximum model space distance between geometric entities at asserted c
onnectivities');
#10481=(
GEOMETRIC_REPRESENTATION_CONTEXT(3)
GLOBAL_UNCERTAINTY_ASSIGNED_CONTEXT((#10442))
GLOBAL_UNIT_ASSIGNED_CONTEXT((#10511,#10513,#10514))
REPRESENTATION_CONTEXT('','3D')
);
#10510=(
GEOMETRIC_REPRESENTATION_CONTEXT(3)
GLOBAL_UNCERTAINTY_ASSIGNED_CONTEXT((#10471))
GLOBAL_UNIT_ASSIGNED_CONTEXT((#10511,#10513,#10514))
REPRESENTATION_CONTEXT('','3D')
);
#10511=(
LENGTH_UNIT()
NAMED_UNIT(*)
SI_UNIT(.CENTI.,.METRE.)
);
#10513=(
NAMED_UNIT(*)
PLANE_ANGLE_UNIT()
SI_UNIT($,.RADIAN.)
);
#10514=(
NAMED_UNIT(*)
SI_UNIT($,.STERADIAN.)
SOLID_ANGLE_UNIT()
);
#10524=SHAPE_DEFINITION_REPRESENTATION(#10562,#10654);
#10562=PRODUCT_DEFINITION_SHAPE('',$,#10693);
#10654=SHAPE_REPRESENTATION('',(#5829),#10481);
#10683=PRODUCT_DEFINITION_CONTEXT('part definition',#10799,'design');
#10693=PRODUCT_DEFINITION('Flat Washer - M6','Flat Washer - M6',#10731,
#10683);
#10731=PRODUCT_DEFINITION_FORMATION('',$,#10810);
#10799=APPLICATION_CONTEXT(
'Core Data for Automotive Mechanical Design Process');
#10800=PRODUCT_CONTEXT('part definition',#10799,'mechanical');
#10810=PRODUCT('Flat Washer - M6','Flat Washer - M6','Flat Washer - M6',
(#10800));
#10909=COLOUR_RGB('Black',0.12,0.14,0.17);
#10910=FILL_AREA_STYLE_COLOUR('',#10909);
#10911=FILL_AREA_STYLE('',(#10910));
#10912=SURFACE_STYLE_FILL_AREA(#10911);
#10913=SURFACE_SIDE_STYLE('',(#10912));
#10914=SURFACE_STYLE_USAGE(.BOTH.,#10913);
#10915=PRESENTATION_STYLE_ASSIGNMENT((#10914));
ENDSEC;
END-ISO-10303-21;
